ISO-10303-21;
HEADER;
FILE_DESCRIPTION (('STEP AP214'),
    '1' );
FILE_NAME ('socket button head screw_iso_ISO 7380 - M4 x 8 - 8N.step',
    '2026-10-04T13:31:42',
    ( '' ),
    ( '' ),
    'SwSTEP 2.0',
    'SolidWorks 2026',
    '' );
FILE_SCHEMA (( 'AUTOMOTIVE_DESIGN' ));
ENDSEC;

DATA;
#36=CARTESIAN_POINT ( 'NONE',  ( 0.000000000000000000, 0.000000000000000000, 0.000000000000000000 ) ) ;
#37=CARTESIAN_POINT ( 'NONE',  ( 0.000000000000000000, -0.7216878364870318308, 1.249999999999999778 ) ) ;
#96=AXIS2_PLACEMENT_3D ( 'NONE', #158680, #174858, #36324 ) ;
#134=CARTESIAN_POINT ( 'NONE',  ( 9.809999999999998721, 0.000000000000000000, 1.999999999999999556 ) ) ;
#174=APPLICATION_CONTEXT ( 'automotive_design' ) ;
#829=EDGE_CURVE ( 'NONE', #120001, #168590, #75101, .T. ) ;
#1352=FACE_OUTER_BOUND ( 'NONE', #80306, .T. ) ;
#1533=VECTOR ( 'NONE', #54192, 1000.000000000000000 ) ;
#1718=CARTESIAN_POINT ( 'NONE',  ( 2.200000000000000178, 4.653657836759941744E-16, -3.799999999999999378 ) ) ;
#2854=VERTEX_POINT ( 'NONE', #99206 ) ;
#3021=ORIENTED_EDGE ( 'NONE', *, *, #106786, .F. ) ;
#3247=VERTEX_POINT ( 'NONE', #81837 ) ;
#3527=CARTESIAN_POINT ( 'NONE',  ( 8.673617379884035472E-16, 1.899999999999999689, 0.000000000000000000 ) ) ;
#4353=FACE_OUTER_BOUND ( 'NONE', #24443, .T. ) ;
#4497=DIRECTION ( 'NONE',  ( -1.000000000000000000, -0.000000000000000000, -0.000000000000000000 ) ) ;
#4794=AXIS2_PLACEMENT_3D ( 'NONE', #35630, #97275, #157983 ) ;
#4921=CIRCLE ( 'NONE', #117974, 3.799999999999999378 ) ;
#4933=EDGE_LOOP ( 'NONE', ( #151041, #193866, #198494, #130742, #179815 ) ) ;
#5623=STYLED_ITEM ( 'NONE', ( #178064 ), #74599 ) ;
#5842=FACE_OUTER_BOUND ( 'NONE', #173760, .T. ) ;
#6214=ORIENTED_EDGE ( 'NONE', *, *, #121040, .F. ) ;
#6387=ORIENTED_EDGE ( 'NONE', *, *, #121040, .T. ) ;
#6418=LINE ( 'NONE', #131782, #102043 ) ;
#6478=ORIENTED_EDGE ( 'NONE', *, *, #129249, .T. ) ;
#6760=ADVANCED_FACE ( 'NONE', ( #38903 ), #132903, .T. ) ;
#7628=ORIENTED_EDGE ( 'NONE', *, *, #49174, .T. ) ;
#7693=AXIS2_PLACEMENT_3D ( 'NONE', #192247, #178083, #22396 ) ;
#8323=DIRECTION ( 'NONE',  ( 0.000000000000000000, 1.000000000000000000, 0.000000000000000000 ) ) ;
#8650=VERTEX_POINT ( 'NONE', #85667 ) ;
#8703=ORIENTED_EDGE ( 'NONE', *, *, #135435, .T. ) ;
#9021=CARTESIAN_POINT ( 'NONE',  ( 1.300000000000000044, 0.000000000000000000, 0.000000000000000000 ) ) ;
#9184=EDGE_CURVE ( 'NONE', #150360, #8650, #151354, .T. ) ;
#9252=DIRECTION ( 'NONE',  ( -1.000000000000000000, -0.000000000000000000, -0.000000000000000000 ) ) ;
#9335=CARTESIAN_POINT ( 'NONE',  ( 2.021687836487040535, 0.000000000000000000, 2.168404344971008868E-16 ) ) ;
#9642=VECTOR ( 'NONE', #178187, 1000.000000000000114 ) ;
#10166=DIRECTION ( 'NONE',  ( -0.000000000000000000, 1.000000000000000000, 1.224646799147353207E-16 ) ) ;
#10290=CARTESIAN_POINT ( 'NONE',  ( 2.021687836487040535, 2.168404344971008868E-16, 0.000000000000000000 ) ) ;
#10351=CARTESIAN_POINT ( 'NONE',  ( 1.300000000000000044, -1.443375672974063884, -3.691112476943992763E-18 ) ) ;
#10609=ORIENTED_EDGE ( 'NONE', *, *, #136319, .F. ) ;
#10964=LINE ( 'NONE', #72638, #92055 ) ;
#11216=DIRECTION ( 'NONE',  ( -1.000000000000000000, 0.000000000000000000, 0.000000000000000000 ) ) ;
#11237=DIRECTION ( 'NONE',  ( -0.000000000000000000, 0.4999999999999998890, -0.8660254037844387076 ) ) ;
#11491=PLANE ( 'NONE',  #79409 ) ;
#11758=VERTEX_POINT ( 'NONE', #134 ) ;
#11787=CARTESIAN_POINT ( 'NONE',  ( 2.400000000000000799, 0.000000000000000000, 1.999999999999999112 ) ) ;
#11794=CARTESIAN_POINT ( 'NONE',  ( 1.300000000000000044, 1.443375672974065216, 7.017607234860990640E-28 ) ) ;
#12030=DIRECTION ( 'NONE',  ( -1.000000000000000000, -0.000000000000000000, -0.000000000000000000 ) ) ;
#12241=FACE_OUTER_BOUND ( 'NONE', #179038, .T. ) ;
#12330=ORIENTED_EDGE ( 'NONE', *, *, #34560, .T. ) ;
#12595=DIRECTION ( 'NONE',  ( -1.000000000000000000, -0.000000000000000000, -0.000000000000000000 ) ) ;
#12655=ORIENTED_EDGE ( 'NONE', *, *, #61124, .F. ) ;
#13078=EDGE_CURVE ( 'NONE', #161515, #82858, #127381, .T. ) ;
#13127=CONICAL_SURFACE ( 'NONE', #54963, 1.610000000000000098, 0.7853981633974458365 ) ;
#13338=EDGE_CURVE ( 'NONE', #194693, #87119, #56395, .T. ) ;
#13448=VERTEX_POINT ( 'NONE', #10290 ) ;
#14245=CARTESIAN_POINT ( 'NONE',  ( 2.400000000000000799, 0.000000000000000000, 2.199999999999999289 ) ) ;
#14429=EDGE_CURVE ( 'NONE', #171876, #150360, #132028, .T. ) ;
#14709=EDGE_CURVE ( 'NONE', #163628, #83320, #66359, .T. ) ;
#15187=CARTESIAN_POINT ( 'NONE',  ( 1.300000000000000044, 0.000000000000000000, 0.000000000000000000 ) ) ;
#15275=CARTESIAN_POINT ( 'NONE',  ( 1.300000000000000044, 0.7216878364870328300, 1.249999999999999778 ) ) ;
#15283=DIRECTION ( 'NONE',  ( 0.000000000000000000, 0.000000000000000000, 1.000000000000000000 ) ) ;
#15931=DIRECTION ( 'NONE',  ( -0.000000000000000000, 0.4999999999999998890, -0.8660254037844387076 ) ) ;
#16442=DIRECTION ( 'NONE',  ( 0.000000000000000000, 0.8660254037844387076, 0.4999999999999998890 ) ) ;
#16981=VERTEX_POINT ( 'NONE', #182292 ) ;
#17675=CARTESIAN_POINT ( 'NONE',  ( 8.673617379884035472E-16, 0.000000000000000000, 0.000000000000000000 ) ) ;
#17734=( GEOMETRIC_REPRESENTATION_CONTEXT ( 3 ) GLOBAL_UNCERTAINTY_ASSIGNED_CONTEXT ( ( #141424 ) ) GLOBAL_UNIT_ASSIGNED_CONTEXT ( ( #198021, #182858, #135370 ) ) REPRESENTATION_CONTEXT ( 'NONE', 'WORKASPACE' ) );
#18223=DIRECTION ( 'NONE',  ( -0.000000000000000000, -1.000000000000000000, -0.000000000000000000 ) ) ;
#18239=CIRCLE ( 'NONE', #44081, 2.199999999999999289 ) ;
#18792=ORIENTED_EDGE ( 'NONE', *, *, #22613, .T. ) ;
#19281=DIRECTION ( 'NONE',  ( 0.000000000000000000, 0.000000000000000000, 1.000000000000000000 ) ) ;
#20577=EDGE_CURVE ( 'NONE', #87119, #172465, #24387, .T. ) ;
#21113=EDGE_LOOP ( 'NONE', ( #146922, #45592, #158394, #58948, #160275 ) ) ;
#21298=ADVANCED_FACE ( 'NONE', ( #64712 ), #108221, .T. ) ;
#21387=CARTESIAN_POINT ( 'NONE',  ( 4.336808689942017736E-16, 0.000000000000000000, 0.000000000000000000 ) ) ;
#21894=DIRECTION ( 'NONE',  ( 0.000000000000000000, 1.224646799147353207E-16, -1.000000000000000000 ) ) ;
#21944=CARTESIAN_POINT ( 'NONE',  ( 8.673617379884035472E-16, -1.899999999999999689, -3.490243377569955075E-16 ) ) ;
#22377=( NAMED_UNIT ( * ) PLANE_ANGLE_UNIT ( ) SI_UNIT ( $, .RADIAN. ) );
#22396=DIRECTION ( 'NONE',  ( 0.000000000000000000, 0.000000000000000000, 1.000000000000000000 ) ) ;
#22613=EDGE_CURVE ( 'NONE', #169869, #120001, #43333, .T. ) ;
#22757=LINE ( 'NONE', #84406, #129264 ) ;
#22950=EDGE_LOOP ( 'NONE', ( #136347, #41835 ) ) ;
#23174=PLANE ( 'NONE',  #160525 ) ;
#23367=ORIENTED_EDGE ( 'NONE', *, *, #829, .T. ) ;
#23495=LINE ( 'NONE', #9335, #9642 ) ;
#23637=UNCERTAINTY_MEASURE_WITH_UNIT (LENGTH_MEASURE( 1.000000000000000082E-05 ), #54703, 'distance_accuracy_value', 'NONE');
#23666=ORIENTED_EDGE ( 'NONE', *, *, #45131, .T. ) ;
#23783=FACE_OUTER_BOUND ( 'NONE', #28695, .T. ) ;
#23898=DIRECTION ( 'NONE',  ( -1.000000000000000000, 0.000000000000000000, -0.000000000000000000 ) ) ;
#24149=EDGE_CURVE ( 'NONE', #100314, #159084, #92500, .T. ) ;
#24387=CIRCLE ( 'NONE', #169250, 1.899999999999999689 ) ;
#24390=SURFACE_SIDE_STYLE ('',( #39532 ) ) ;
#24443=EDGE_LOOP ( 'NONE', ( #191036, #51219, #183121 ) ) ;
#24598=AXIS2_PLACEMENT_3D ( 'NONE', #73668, #196026, #165670 ) ;
#24751=DIRECTION ( 'NONE',  ( 0.000000000000000000, -0.8660254037844385966, 0.5000000000000001110 ) ) ;
#24794=PLANE ( 'NONE',  #192677 ) ;
#25024=CARTESIAN_POINT ( 'NONE',  ( 1.300000000000000044, -0.7216878364870318308, 1.249999999999999778 ) ) ;
#25208=SHAPE_REPRESENTATION_RELATIONSHIP ( 'NONE' , 'NONE' ,  #71529, #51975 ) ;
#25227=ORIENTED_EDGE ( 'NONE', *, *, #106983, .T. ) ;
#25328=DIRECTION ( 'NONE',  ( 0.000000000000000000, 0.000000000000000000, 1.000000000000000000 ) ) ;
#25417=PLANE ( 'NONE',  #165918 ) ;
#25508=DIRECTION ( 'NONE',  ( -1.000000000000000000, 0.000000000000000000, 0.000000000000000000 ) ) ;
#26019=ORIENTED_EDGE ( 'NONE', *, *, #129249, .F. ) ;
#26170=DIRECTION ( 'NONE',  ( -1.000000000000000000, -0.000000000000000000, -0.000000000000000000 ) ) ;
#26619=CARTESIAN_POINT ( 'NONE',  ( 10.20000000000000107, 0.000000000000000000, 0.000000000000000000 ) ) ;
#27456=AXIS2_PLACEMENT_3D ( 'NONE', #158408, #21894, #160405 ) ;
#27500=DIRECTION ( 'NONE',  ( -1.000000000000000000, -0.000000000000000000, -0.000000000000000000 ) ) ;
#27642=DIRECTION ( 'NONE',  ( -0.000000000000000000, 1.000000000000000000, -0.000000000000000000 ) ) ;
#28201=SURFACE_STYLE_USAGE ( .BOTH. , #58508 ) ;
#28526=DIRECTION ( 'NONE',  ( -0.000000000000000000, 0.5000000000000001110, 0.8660254037844385966 ) ) ;
#28695=EDGE_LOOP ( 'NONE', ( #73188, #180107, #173277 ) ) ;
#28846=VECTOR ( 'NONE', #56608, 1000.000000000000000 ) ;
#29175=CYLINDRICAL_SURFACE ( 'NONE', #69279, 3.799999999999999378 ) ;
#29688=EDGE_CURVE ( 'NONE', #166995, #120001, #127476, .T. ) ;
#29730=LINE ( 'NONE', #153054, #85508 ) ;
#29924=EDGE_CURVE ( 'NONE', #168590, #83320, #173162, .T. ) ;
#30091=VECTOR ( 'NONE', #145579, 1000.000000000000114 ) ;
#30230=DIRECTION ( 'NONE',  ( 0.000000000000000000, 0.000000000000000000, 1.000000000000000000 ) ) ;
#30398=AXIS2_PLACEMENT_3D ( 'NONE', #128371, #143538, #51543 ) ;
#30422=CLOSED_SHELL ( 'NONE', ( #154540, #106869, #89797, #21298, #65004, #129684, #197689, #91262, #49601, #185178, #189850, #186823, #58481, #71549, #36411, #60710, #65126, #6760, #116252, #152511, #62467, #63405, #110107, #107491, #169227, #194656, #141333 ) ) ;
#30542=AXIS2_PLACEMENT_3D ( 'NONE', #147678, #10166, #58645 ) ;
#31306=DIRECTION ( 'NONE',  ( -0.5000000000000044409, 1.060575238724903587E-16, -0.8660254037844360431 ) ) ;
#32015=ORIENTED_EDGE ( 'NONE', *, *, #106786, .T. ) ;
#32305=FACE_OUTER_BOUND ( 'NONE', #74325, .T. ) ;
#33088=LINE ( 'NONE', #154437, #169434 ) ;
#33593=DIRECTION ( 'NONE',  ( 0.000000000000000000, 0.000000000000000000, 1.000000000000000000 ) ) ;
#33738=AXIS2_PLACEMENT_3D ( 'NONE', #72236, #24751, #162240 ) ;
#33802=CARTESIAN_POINT ( 'NONE',  ( 1.820000000000000062, 0.000000000000000000, 0.000000000000000000 ) ) ;
#34243=CIRCLE ( 'NONE', #147258, 1.249999999999999778 ) ;
#34252=UNCERTAINTY_MEASURE_WITH_UNIT (LENGTH_MEASURE( 1.000000000000000082E-05 ), #151525, 'distance_accuracy_value', 'NONE');
#34358=DIRECTION ( 'NONE',  ( -1.000000000000000000, 0.000000000000000000, 0.000000000000000000 ) ) ;
#34560=EDGE_CURVE ( 'NONE', #86859, #100314, #29730, .T. ) ;
#34569=FACE_OUTER_BOUND ( 'NONE', #42514, .T. ) ;
#35005=VERTEX_POINT ( 'NONE', #96343 ) ;
#35466=AXIS2_PLACEMENT_3D ( 'NONE', #125460, #144591, #19281 ) ;
#35542=FILL_AREA_STYLE_COLOUR ( '', #147681 ) ;
#35630=CARTESIAN_POINT ( 'NONE',  ( 1.300000000000000044, 0.000000000000000000, 0.000000000000000000 ) ) ;
#35771=CARTESIAN_POINT ( 'NONE',  ( 0.000000000000000000, 2.449293598294705428E-16, -1.999999999999999112 ) ) ;
#36053=PLANE ( 'NONE',  #185756 ) ;
#36324=DIRECTION ( 'NONE',  ( 0.000000000000000000, 0.000000000000000000, 1.000000000000000000 ) ) ;
#36411=ADVANCED_FACE ( 'NONE', ( #163018 ), #88167, .T. ) ;
#36640=DIRECTION ( 'NONE',  ( 0.000000000000000000, 0.000000000000000000, -1.000000000000000000 ) ) ;
#36768=CARTESIAN_POINT ( 'NONE',  ( 10.20000000000000107, 0.000000000000000000, 1.610000000000000098 ) ) ;
#36883=LINE ( 'NONE', #15275, #37456 ) ;
#37224=ORIENTED_EDGE ( 'NONE', *, *, #65894, .T. ) ;
#37456=VECTOR ( 'NONE', #199302, 1000.000000000000114 ) ;
#37588=ORIENTED_EDGE ( 'NONE', *, *, #57273, .T. ) ;
#37698=CIRCLE ( 'NONE', #70043, 1.999999999999999112 ) ;
#37703=EDGE_CURVE ( 'NONE', #54292, #83313, #98474, .T. ) ;
#37804=AXIS2_PLACEMENT_3D ( 'NONE', #119849, #149198, #58182 ) ;
#37985=ORIENTED_EDGE ( 'NONE', *, *, #137680, .T. ) ;
#38115=VECTOR ( 'NONE', #153443, 999.9999999999998863 ) ;
#38253=VECTOR ( 'NONE', #194788, 1000.000000000000114 ) ;
#38353=ORIENTED_EDGE ( 'NONE', *, *, #173030, .T. ) ;
#38471=ORIENTED_EDGE ( 'NONE', *, *, #61495, .F. ) ;
#38494=CARTESIAN_POINT ( 'NONE',  ( 1.300000000000000044, 0.000000000000000000, 0.000000000000000000 ) ) ;
#38903=FACE_OUTER_BOUND ( 'NONE', #154987, .T. ) ;
#38944=CARTESIAN_POINT ( 'NONE',  ( 1.300000000000000044, 0.7216878364870328300, -1.250000000000000000 ) ) ;
#39003=EDGE_CURVE ( 'NONE', #86859, #41998, #36883, .T. ) ;
#39532=SURFACE_STYLE_FILL_AREA ( #108404 ) ;
#39552=DIRECTION ( 'NONE',  ( -1.000000000000000000, -0.000000000000000000, -0.000000000000000000 ) ) ;
#39647=DIRECTION ( 'NONE',  ( 0.000000000000000000, -0.8660254037844385966, -0.5000000000000003331 ) ) ;
#39791=ORIENTED_EDGE ( 'NONE', *, *, #73698, .F. ) ;
#40428=SPHERICAL_SURFACE ( 'NONE', #61444, 4.324969328314201888 ) ;
#40568=ORIENTED_EDGE ( 'NONE', *, *, #118900, .F. ) ;
#40653=DIRECTION ( 'NONE',  ( 0.000000000000000000, 0.000000000000000000, 1.000000000000000000 ) ) ;
#40775=DIRECTION ( 'NONE',  ( -1.000000000000000000, -0.000000000000000000, -0.000000000000000000 ) ) ;
#41254=LINE ( 'NONE', #178775, #108027 ) ;
#41797=CARTESIAN_POINT ( 'NONE',  ( 1.300000000000000044, 0.7216878364870328300, -1.250000000000000000 ) ) ;
#41816=CARTESIAN_POINT ( 'NONE',  ( 1.300000000000000044, -0.7216878364870318308, 1.249999999999999778 ) ) ;
#41835=ORIENTED_EDGE ( 'NONE', *, *, #132614, .F. ) ;
#41998=VERTEX_POINT ( 'NONE', #199678 ) ;
#42514=EDGE_LOOP ( 'NONE', ( #152231, #142466 ) ) ;
#43333=LINE ( 'NONE', #90805, #162401 ) ;
#43466=CARTESIAN_POINT ( 'NONE',  ( 9.809999999999998721, 0.000000000000000000, 0.000000000000000000 ) ) ;
#44081=AXIS2_PLACEMENT_3D ( 'NONE', #161920, #9252, #68909 ) ;
#45131=EDGE_CURVE ( 'NONE', #166995, #86859, #100843, .T. ) ;
#45202=VERTEX_POINT ( 'NONE', #137921 ) ;
#45302=CIRCLE ( 'NONE', #96, 1.999999999999999112 ) ;
#45588=DIRECTION ( 'NONE',  ( 1.000000000000000000, 0.000000000000000000, 0.000000000000000000 ) ) ;
#45592=ORIENTED_EDGE ( 'NONE', *, *, #186506, .T. ) ;
#46111=CIRCLE ( 'NONE', #159091, 1.999999999999999556 ) ;
#46214=VECTOR ( 'NONE', #61172, 1000.000000000000114 ) ;
#46251=CYLINDRICAL_SURFACE ( 'NONE', #81775, 1.999999999999999112 ) ;
#46884=DIRECTION ( 'NONE',  ( -1.000000000000000000, -0.000000000000000000, -0.000000000000000000 ) ) ;
#47094=VECTOR ( 'NONE', #183435, 1000.000000000000000 ) ;
#47313=ORIENTED_EDGE ( 'NONE', *, *, #85455, .T. ) ;
#47527=AXIS2_PLACEMENT_3D ( 'NONE', #68177, #53005, #113674 ) ;
#48425=ORIENTED_EDGE ( 'NONE', *, *, #140289, .T. ) ;
#48474=LINE ( 'NONE', #108131, #99308 ) ;
#48716=CARTESIAN_POINT ( 'NONE',  ( 10.20000000000000107, 2.210487472460972205E-16, -1.610000000000000098 ) ) ;
#48815=ORIENTED_EDGE ( 'NONE', *, *, #173030, .F. ) ;
#49174=EDGE_CURVE ( 'NONE', #120001, #149477, #117795, .T. ) ;
#49524=FACE_OUTER_BOUND ( 'NONE', #130766, .T. ) ;
#49601=ADVANCED_FACE ( 'NONE', ( #182852 ), #29175, .T. ) ;
#51219=ORIENTED_EDGE ( 'NONE', *, *, #14429, .F. ) ;
#51543=DIRECTION ( 'NONE',  ( 0.000000000000000000, 0.000000000000000000, 1.000000000000000000 ) ) ;
#51964=ORIENTED_EDGE ( 'NONE', *, *, #154401, .T. ) ;
#51975=ADVANCED_BREP_SHAPE_REPRESENTATION ( '', ( #74599, #82054 ), #17734 ) ;
#52593=CARTESIAN_POINT ( 'NONE',  ( 1.300000000000000044, -0.7216878364870318308, 1.249999999999999778 ) ) ;
#52715=CARTESIAN_POINT ( 'NONE',  ( 1.300000000000000044, -0.7216878364870318308, -1.250000000000000000 ) ) ;
#52864=VECTOR ( 'NONE', #11237, 1000.000000000000114 ) ;
#52925=DIRECTION ( 'NONE',  ( -1.000000000000000000, -0.000000000000000000, -0.000000000000000000 ) ) ;
#53005=DIRECTION ( 'NONE',  ( 0.000000000000000000, 0.000000000000000000, 1.000000000000000000 ) ) ;
#53057=AXIS2_PLACEMENT_3D ( 'NONE', #14245, #165964, #134636 ) ;
#53710=( NAMED_UNIT ( * ) SI_UNIT ( $, .STERADIAN. ) SOLID_ANGLE_UNIT ( ) );
#53728=CARTESIAN_POINT ( 'NONE',  ( 2.400000000000000799, 0.000000000000000000, 0.000000000000000000 ) ) ;
#53832=EDGE_CURVE ( 'NONE', #117197, #194693, #56586, .T. ) ;
#54192=DIRECTION ( 'NONE',  ( -0.000000000000000000, 1.000000000000000000, -0.000000000000000000 ) ) ;
#54292=VERTEX_POINT ( 'NONE', #36768 ) ;
#54535=CARTESIAN_POINT ( 'NONE',  ( 0.000000000000000000, 0.000000000000000000, 3.799999999999999378 ) ) ;
#54576=LINE ( 'NONE', #129401, #30091 ) ;
#54703=( LENGTH_UNIT ( ) NAMED_UNIT ( * ) SI_UNIT ( .MILLI., .METRE. ) );
#54963=AXIS2_PLACEMENT_3D ( 'NONE', #192610, #12595, #72259 ) ;
#55668=ORIENTED_EDGE ( 'NONE', *, *, #37703, .T. ) ;
#55815=FACE_OUTER_BOUND ( 'NONE', #73387, .T. ) ;
#55818=ORIENTED_EDGE ( 'NONE', *, *, #57511, .F. ) ;
#55953=ORIENTED_EDGE ( 'NONE', *, *, #29924, .T. ) ;
#56395=CIRCLE ( 'NONE', #153230, 4.324969328314201888 ) ;
#56586=CIRCLE ( 'NONE', #166302, 3.799999999999999378 ) ;
#56608=DIRECTION ( 'NONE',  ( -0.000000000000000000, -1.000000000000000000, -0.000000000000000000 ) ) ;
#57273=EDGE_CURVE ( 'NONE', #144758, #89112, #10964, .T. ) ;
#57511=EDGE_CURVE ( 'NONE', #149477, #169869, #33088, .T. ) ;
#57708=EDGE_CURVE ( 'NONE', #185003, #172465, #62907, .T. ) ;
#57850=DIRECTION ( 'NONE',  ( 0.000000000000000000, 0.4999999999999999445, 0.8660254037844387076 ) ) ;
#58137=CIRCLE ( 'NONE', #116264, 1.610000000000000098 ) ;
#58182=DIRECTION ( 'NONE',  ( -0.000000000000000000, 0.000000000000000000, 1.000000000000000000 ) ) ;
#58438=FACE_OUTER_BOUND ( 'NONE', #138008, .T. ) ;
#58481=ADVANCED_FACE ( 'NONE', ( #174588 ), #36053, .F. ) ;
#58508=SURFACE_SIDE_STYLE ('',( #86850 ) ) ;
#58645=DIRECTION ( 'NONE',  ( 0.000000000000000000, -1.224646799147353207E-16, 1.000000000000000000 ) ) ;
#58761=DIRECTION ( 'NONE',  ( 0.000000000000000000, 0.000000000000000000, 1.000000000000000000 ) ) ;
#58948=ORIENTED_EDGE ( 'NONE', *, *, #78126, .F. ) ;
#58961=PLANE ( 'NONE',  #124739 ) ;
#59004=ORIENTED_EDGE ( 'NONE', *, *, #174899, .T. ) ;
#59169=DIRECTION ( 'NONE',  ( 0.000000000000000000, 0.000000000000000000, 1.000000000000000000 ) ) ;
#59910=FACE_OUTER_BOUND ( 'NONE', #65662, .T. ) ;
#60489=ORIENTED_EDGE ( 'NONE', *, *, #112510, .T. ) ;
#60710=ADVANCED_FACE ( 'NONE', ( #137787 ), #58961, .T. ) ;
#60809=LINE ( 'NONE', #94129, #92491 ) ;
#61124=EDGE_CURVE ( 'NONE', #41998, #166995, #140895, .T. ) ;
#61172=DIRECTION ( 'NONE',  ( -0.000000000000000000, -0.5000000000000002220, 0.8660254037844384856 ) ) ;
#61444=AXIS2_PLACEMENT_3D ( 'NONE', #191114, #146590, #193116 ) ;
#61495=EDGE_CURVE ( 'NONE', #161515, #182913, #18239, .T. ) ;
#61713=ORIENTED_EDGE ( 'NONE', *, *, #162564, .T. ) ;
#61806=CARTESIAN_POINT ( 'NONE',  ( 1.300000000000000044, -0.7216878364870318308, 1.249999999999999778 ) ) ;
#61968=ORIENTED_EDGE ( 'NONE', *, *, #167140, .F. ) ;
#62467=ADVANCED_FACE ( 'NONE', ( #49524 ), #113171, .T. ) ;
#62850=CIRCLE ( 'NONE', #117721, 1.249999999999999778 ) ;
#62907=CIRCLE ( 'NONE', #27456, 4.324969328314201888 ) ;
#63405=ADVANCED_FACE ( 'NONE', ( #175859 ), #23174, .T. ) ;
#63675=DIRECTION ( 'NONE',  ( -1.000000000000000000, -0.000000000000000000, -0.000000000000000000 ) ) ;
#64144=DIRECTION ( 'NONE',  ( -1.000000000000000000, -0.000000000000000000, -0.000000000000000000 ) ) ;
#64526=ORIENTED_EDGE ( 'NONE', *, *, #20577, .F. ) ;
#64712=FACE_OUTER_BOUND ( 'NONE', #117346, .T. ) ;
#65004=ADVANCED_FACE ( 'NONE', ( #191528 ), #145016, .T. ) ;
#65126=ADVANCED_FACE ( 'NONE', ( #176379 ), #146015, .T. ) ;
#65570=EDGE_CURVE ( 'NONE', #2854, #117197, #174380, .T. ) ;
#65662=EDGE_LOOP ( 'NONE', ( #106259, #6387, #132538, #133049 ) ) ;
#65894=EDGE_CURVE ( 'NONE', #191214, #82858, #37698, .T. ) ;
#66038=PLANE ( 'NONE',  #178825 ) ;
#66064=( GEOMETRIC_REPRESENTATION_CONTEXT ( 3 ) GLOBAL_UNCERTAINTY_ASSIGNED_CONTEXT ( ( #34252 ) ) GLOBAL_UNIT_ASSIGNED_CONTEXT ( ( #151525, #74679, #194053 ) ) REPRESENTATION_CONTEXT ( 'NONE', 'WORKASPACE' ) );
#66083=AXIS2_PLACEMENT_3D ( 'NONE', #9021, #70689, #97986 ) ;
#66119=DIRECTION ( 'NONE',  ( 0.000000000000000000, 0.000000000000000000, 1.000000000000000000 ) ) ;
#66359=LINE ( 'NONE', #163374, #1533 ) ;
#66525=CARTESIAN_POINT ( 'NONE',  ( -997.9783121635130101, 0.000000000000000000, 0.000000000000000000 ) ) ;
#66935=VECTOR ( 'NONE', #162181, 1000.000000000000000 ) ;
#67759=VECTOR ( 'NONE', #157393, 1000.000000000000000 ) ;
#67906=CARTESIAN_POINT ( 'NONE',  ( 1.300000000000000044, 0.000000000000000000, 0.000000000000000000 ) ) ;
#68177=CARTESIAN_POINT ( 'NONE',  ( 1.300000000000000044, 0.7216878364870328300, -1.250000000000000000 ) ) ;
#68247=CARTESIAN_POINT ( 'NONE',  ( 1.820000000000000062, 4.653657836759941744E-16, -3.799999999999999378 ) ) ;
#68895=ORIENTED_EDGE ( 'NONE', *, *, #174899, .F. ) ;
#68909=DIRECTION ( 'NONE',  ( 0.000000000000000000, 0.000000000000000000, 1.000000000000000000 ) ) ;
#69129=ORIENTED_EDGE ( 'NONE', *, *, #167140, .T. ) ;
#69279=AXIS2_PLACEMENT_3D ( 'NONE', #151519, #12030, #119193 ) ;
#69562=DIRECTION ( 'NONE',  ( -1.000000000000000000, -0.000000000000000000, -0.000000000000000000 ) ) ;
#70043=AXIS2_PLACEMENT_3D ( 'NONE', #113202, #146529, #99021 ) ;
#70586=DIRECTION ( 'NONE',  ( -0.7071067811865492381, 8.659560562354911904E-17, -0.7071067811865457964 ) ) ;
#70689=DIRECTION ( 'NONE',  ( -1.000000000000000000, -0.000000000000000000, -0.000000000000000000 ) ) ;
#71128=ORIENTED_EDGE ( 'NONE', *, *, #829, .F. ) ;
#71529=SHAPE_REPRESENTATION ( 'socket button head screw_iso_ISO 7380 - M4 x 8 - 8N', ( #82054 ), #17734 ) ;
#71549=ADVANCED_FACE ( 'NONE', ( #32305 ), #157356, .F. ) ;
#71748=EDGE_CURVE ( 'NONE', #13448, #120001, #48474, .T. ) ;
#71991=DIRECTION ( 'NONE',  ( 0.000000000000000000, 0.000000000000000000, 1.000000000000000000 ) ) ;
#72236=CARTESIAN_POINT ( 'NONE',  ( 1.300000000000000044, 1.443375672974065216, 7.017607234860990640E-28 ) ) ;
#72259=DIRECTION ( 'NONE',  ( 0.000000000000000000, 0.000000000000000000, 1.000000000000000000 ) ) ;
#72638=CARTESIAN_POINT ( 'NONE',  ( 0.000000000000000000, 4.653657836759941744E-16, -3.799999999999999378 ) ) ;
#73188=ORIENTED_EDGE ( 'NONE', *, *, #106983, .F. ) ;
#73387=EDGE_LOOP ( 'NONE', ( #48815, #71128, #182253 ) ) ;
#73668=CARTESIAN_POINT ( 'NONE',  ( -997.9783121635130101, 0.000000000000000000, 0.000000000000000000 ) ) ;
#73698=EDGE_CURVE ( 'NONE', #54292, #11758, #76072, .T. ) ;
#73874=ORIENTED_EDGE ( 'NONE', *, *, #57511, .T. ) ;
#74325=EDGE_LOOP ( 'NONE', ( #10609, #38471, #139930, #115678 ) ) ;
#74599=MANIFOLD_SOLID_BREP ( 'Hex', #30422 ) ;
#74679=( NAMED_UNIT ( * ) PLANE_ANGLE_UNIT ( ) SI_UNIT ( $, .RADIAN. ) );
#74972=CARTESIAN_POINT ( 'NONE',  ( 1.820000000000000062, 0.000000000000000000, 3.799999999999999378 ) ) ;
#75060=ORIENTED_EDGE ( 'NONE', *, *, #37703, .F. ) ;
#75101=LINE ( 'NONE', #41797, #172887 ) ;
#75719=EDGE_CURVE ( 'NONE', #35005, #159084, #88029, .T. ) ;
#75844=AXIS2_PLACEMENT_3D ( 'NONE', #10351, #134698, #57850 ) ;
#76072=LINE ( 'NONE', #133782, #180036 ) ;
#76708=ORIENTED_EDGE ( 'NONE', *, *, #90570, .F. ) ;
#77748=ORIENTED_EDGE ( 'NONE', *, *, #157667, .T. ) ;
#78126=EDGE_CURVE ( 'NONE', #8650, #45202, #167632, .T. ) ;
#79146=DIRECTION ( 'NONE',  ( -1.000000000000000000, 0.000000000000000000, 0.000000000000000000 ) ) ;
#79264=DIRECTION ( 'NONE',  ( -1.000000000000000000, -0.000000000000000000, -0.000000000000000000 ) ) ;
#79409=AXIS2_PLACEMENT_3D ( 'NONE', #41816, #150994, #146986 ) ;
#79790=CARTESIAN_POINT ( 'NONE',  ( 2.400000000000000799, 0.000000000000000000, 0.000000000000000000 ) ) ;
#79862=CARTESIAN_POINT ( 'NONE',  ( 1.300000000000000044, -0.7216878364870319418, 1.249999999999999778 ) ) ;
#80306=EDGE_LOOP ( 'NONE', ( #141979, #48425, #97620, #80680, #122632 ) ) ;
#80316=DIRECTION ( 'NONE',  ( 0.000000000000000000, 0.000000000000000000, 1.000000000000000000 ) ) ;
#80680=ORIENTED_EDGE ( 'NONE', *, *, #13338, .T. ) ;
#81190=CARTESIAN_POINT ( 'NONE',  ( 2.400000000000000799, 2.449293598294705428E-16, -1.999999999999999112 ) ) ;
#81775=AXIS2_PLACEMENT_3D ( 'NONE', #169591, #120106, #181796 ) ;
#81837=CARTESIAN_POINT ( 'NONE',  ( 1.300000000000000044, -1.443375672974063884, -3.691112476943992763E-18 ) ) ;
#81845=DIRECTION ( 'NONE',  ( -1.000000000000000000, -0.000000000000000000, -0.000000000000000000 ) ) ;
#82054=AXIS2_PLACEMENT_3D ( 'NONE', #82060, #99242, #83075 ) ;
#82060=CARTESIAN_POINT ( 'NONE',  ( 0.000000000000000000, 0.000000000000000000, 0.000000000000000000 ) ) ;
#82207=STYLED_ITEM ( 'NONE', ( #178881 ), #51975 ) ;
#82546=CARTESIAN_POINT ( 'NONE',  ( 10.20000000000000107, 0.000000000000000000, 0.000000000000000000 ) ) ;
#82858=VERTEX_POINT ( 'NONE', #11787 ) ;
#83045=DIRECTION ( 'NONE',  ( -1.000000000000000000, 0.000000000000000000, -0.000000000000000000 ) ) ;
#83075=DIRECTION ( 'NONE',  ( 1.000000000000000000, 0.000000000000000000, 0.000000000000000000 ) ) ;
#83313=VERTEX_POINT ( 'NONE', #48716 ) ;
#83320=VERTEX_POINT ( 'NONE', #174055 ) ;
#84324=LINE ( 'NONE', #191516, #66935 ) ;
#84406=CARTESIAN_POINT ( 'NONE',  ( 1.300000000000000044, -1.443375672974063884, -3.691112476943992763E-18 ) ) ;
#84415=ORIENTED_EDGE ( 'NONE', *, *, #110780, .T. ) ;
#84494=CARTESIAN_POINT ( 'NONE',  ( 1.820000000000000062, -3.800000000000000266, -4.653657836759940757E-16 ) ) ;
#84671=CARTESIAN_POINT ( 'NONE',  ( 1.300000000000000044, 1.443375672974065216, 7.017607234860990640E-28 ) ) ;
#84904=AXIS2_PLACEMENT_3D ( 'NONE', #179185, #25508, #40653 ) ;
#84987=VERTEX_POINT ( 'NONE', #141287 ) ;
#85433=CARTESIAN_POINT ( 'NONE',  ( 1.300000000000000044, -0.7216878364870319418, 1.249999999999999778 ) ) ;
#85455=EDGE_CURVE ( 'NONE', #45202, #163628, #178622, .T. ) ;
#85488=ORIENTED_EDGE ( 'NONE', *, *, #34560, .F. ) ;
#85508=VECTOR ( 'NONE', #138879, 1000.000000000000000 ) ;
#85551=DIRECTION ( 'NONE',  ( -0.000000000000000000, 0.000000000000000000, 1.000000000000000000 ) ) ;
#85667=CARTESIAN_POINT ( 'NONE',  ( 4.336808689942017736E-16, -0.7216878364870318308, 1.249999999999999778 ) ) ;
#85680=DIRECTION ( 'NONE',  ( -1.000000000000000000, -0.000000000000000000, -0.000000000000000000 ) ) ;
#86570=ORIENTED_EDGE ( 'NONE', *, *, #147245, .F. ) ;
#86850=SURFACE_STYLE_FILL_AREA ( #149526 ) ;
#86859=VERTEX_POINT ( 'NONE', #188569 ) ;
#87059=DIRECTION ( 'NONE',  ( 0.000000000000000000, 0.000000000000000000, 1.000000000000000000 ) ) ;
#87077=ORIENTED_EDGE ( 'NONE', *, *, #49174, .F. ) ;
#87114=CARTESIAN_POINT ( 'NONE',  ( 3.885274725274726393, -8.673617379884035472E-16, 0.000000000000000000 ) ) ;
#87119=VERTEX_POINT ( 'NONE', #3527 ) ;
#87847=ORIENTED_EDGE ( 'NONE', *, *, #85455, .F. ) ;
#88029=LINE ( 'NONE', #149717, #115475 ) ;
#88167=PLANE ( 'NONE',  #75844 ) ;
#88498=EDGE_CURVE ( 'NONE', #82858, #191214, #45302, .T. ) ;
#89104=EDGE_CURVE ( 'NONE', #150360, #84987, #22757, .T. ) ;
#89112=VERTEX_POINT ( 'NONE', #68247 ) ;
#89385=AXIS2_PLACEMENT_3D ( 'NONE', #144022, #4497, #111703 ) ;
#89505=FACE_BOUND ( 'NONE', #101247, .T. ) ;
#89652=MECHANICAL_DESIGN_GEOMETRIC_PRESENTATION_REPRESENTATION('',(#5623),#189672);
#89797=ADVANCED_FACE ( 'NONE', ( #194614 ), #13127, .T. ) ;
#90246=CARTESIAN_POINT ( 'NONE',  ( 1.300000000000000044, 0.000000000000000000, 1.249999999999999778 ) ) ;
#90385=CARTESIAN_POINT ( 'NONE',  ( 0.000000000000000000, 1.443375672974065216, 7.017607234860990640E-28 ) ) ;
#90570=EDGE_CURVE ( 'NONE', #182913, #161515, #122788, .T. ) ;
#90805=CARTESIAN_POINT ( 'NONE',  ( 1.300000000000000044, 0.7216878364870328300, -1.250000000000000000 ) ) ;
#91262=ADVANCED_FACE ( 'NONE', ( #1352 ), #40428, .T. ) ;
#91772=CARTESIAN_POINT ( 'NONE',  ( 1.300000000000000044, 0.000000000000000000, 0.000000000000000000 ) ) ;
#92055=VECTOR ( 'NONE', #134313, 1000.000000000000000 ) ;
#92491=VECTOR ( 'NONE', #28526, 1000.000000000000000 ) ;
#92500=LINE ( 'NONE', #106689, #46214 ) ;
#93044=DIRECTION ( 'NONE',  ( 0.000000000000000000, 0.000000000000000000, 1.000000000000000000 ) ) ;
#94129=CARTESIAN_POINT ( 'NONE',  ( 0.000000000000000000, 1.443375672974065216, 7.017607234860990640E-28 ) ) ;
#94878=CARTESIAN_POINT ( 'NONE',  ( 1.820000000000000062, 0.000000000000000000, 0.000000000000000000 ) ) ;
#95409=EDGE_CURVE ( 'NONE', #171876, #41998, #109658, .T. ) ;
#95511=ORIENTED_EDGE ( 'NONE', *, *, #112510, .F. ) ;
#96343=CARTESIAN_POINT ( 'NONE',  ( 1.300000000000000044, 0.7216878364870328300, 1.249999999999999778 ) ) ;
#96474=DIRECTION ( 'NONE',  ( -1.000000000000000000, -0.000000000000000000, -0.000000000000000000 ) ) ;
#96593=ORIENTED_EDGE ( 'NONE', *, *, #61124, .T. ) ;
#96641=EDGE_LOOP ( 'NONE', ( #76708, #123014, #123310, #116344 ) ) ;
#97275=DIRECTION ( 'NONE',  ( -1.000000000000000000, -0.000000000000000000, -0.000000000000000000 ) ) ;
#97391=DIRECTION ( 'NONE',  ( 0.000000000000000000, 0.000000000000000000, 1.000000000000000000 ) ) ;
#97415=EDGE_LOOP ( 'NONE', ( #26019, #196735, #7628, #51964, #8703 ) ) ;
#97620=ORIENTED_EDGE ( 'NONE', *, *, #53832, .T. ) ;
#97831=DIRECTION ( 'NONE',  ( 0.000000000000000000, 0.000000000000000000, 1.000000000000000000 ) ) ;
#97986=DIRECTION ( 'NONE',  ( 0.000000000000000000, 0.000000000000000000, 1.000000000000000000 ) ) ;
#98375=MECHANICAL_DESIGN_GEOMETRIC_PRESENTATION_REPRESENTATION('',(#82207),#66064);
#98474=CIRCLE ( 'NONE', #176026, 1.610000000000000098 ) ;
#99021=DIRECTION ( 'NONE',  ( 0.000000000000000000, 0.000000000000000000, 1.000000000000000000 ) ) ;
#99023=VECTOR ( 'NONE', #81845, 1000.000000000000000 ) ;
#99206=CARTESIAN_POINT ( 'NONE',  ( 2.200000000000000178, 0.000000000000000000, 3.799999999999999378 ) ) ;
#99242=DIRECTION ( 'NONE',  ( 0.000000000000000000, 0.000000000000000000, 1.000000000000000000 ) ) ;
#99308=VECTOR ( 'NONE', #31306, 1000.000000000000114 ) ;
#99796=EDGE_CURVE ( 'NONE', #89112, #185003, #132327, .T. ) ;
#100150=DIRECTION ( 'NONE',  ( -1.000000000000000000, -0.000000000000000000, -0.000000000000000000 ) ) ;
#100237=ORIENTED_EDGE ( 'NONE', *, *, #186207, .F. ) ;
#100314=VERTEX_POINT ( 'NONE', #90385 ) ;
#100843=LINE ( 'NONE', #84671, #178993 ) ;
#101141=DIRECTION ( 'NONE',  ( 0.000000000000000000, 0.000000000000000000, 1.000000000000000000 ) ) ;
#101247=EDGE_LOOP ( 'NONE', ( #183333, #180891 ) ) ;
#101308=DIRECTION ( 'NONE',  ( 0.000000000000000000, 0.5000000000000002220, -0.8660254037844384856 ) ) ;
#102043=VECTOR ( 'NONE', #161113, 999.9999999999998863 ) ;
#102142=DIRECTION ( 'NONE',  ( -1.000000000000000000, -0.000000000000000000, -0.000000000000000000 ) ) ;
#102322=CIRCLE ( 'NONE', #186332, 1.999999999999999556 ) ;
#103014=PRODUCT_DEFINITION ( 'UNKNOWN', '', #163074, #143394 ) ;
#103415=ORIENTED_EDGE ( 'NONE', *, *, #22613, .F. ) ;
#103912=ORIENTED_EDGE ( 'NONE', *, *, #39003, .T. ) ;
#105896=CARTESIAN_POINT ( 'NONE',  ( 2.200000000000000622, 2.694222958124176020E-16, -2.199999999999999289 ) ) ;
#105926=ORIENTED_EDGE ( 'NONE', *, *, #29688, .T. ) ;
#106259=ORIENTED_EDGE ( 'NONE', *, *, #137680, .F. ) ;
#106689=CARTESIAN_POINT ( 'NONE',  ( 0.000000000000000000, 0.7216878364870328300, 1.249999999999999778 ) ) ;
#106786=EDGE_CURVE ( 'NONE', #194693, #89112, #182078, .T. ) ;
#106869=ADVANCED_FACE ( 'NONE', ( #131564 ), #198234, .F. ) ;
#106983=EDGE_CURVE ( 'NONE', #3247, #149477, #130550, .T. ) ;
#107220=DIRECTION ( 'NONE',  ( -1.000000000000000000, -0.000000000000000000, -0.000000000000000000 ) ) ;
#107491=ADVANCED_FACE ( 'NONE', ( #12241 ), #25417, .T. ) ;
#108027=VECTOR ( 'NONE', #70586, 1000.000000000000000 ) ;
#108131=CARTESIAN_POINT ( 'NONE',  ( 2.021687836487040535, 2.655529440325959183E-32, -2.168404344971008868E-16 ) ) ;
#108221=CYLINDRICAL_SURFACE ( 'NONE', #143393, 1.999999999999999112 ) ;
#108404=FILL_AREA_STYLE ('',( #35542 ) ) ;
#108486=ORIENTED_EDGE ( 'NONE', *, *, #78126, .T. ) ;
#109658=CIRCLE ( 'NONE', #132186, 1.249999999999999778 ) ;
#110107=ADVANCED_FACE ( 'NONE', ( #55815 ), #117488, .T. ) ;
#110780=EDGE_CURVE ( 'NONE', #16981, #11758, #46111, .T. ) ;
#111703=DIRECTION ( 'NONE',  ( 0.000000000000000000, 0.000000000000000000, 1.000000000000000000 ) ) ;
#112020=ORIENTED_EDGE ( 'NONE', *, *, #13338, .F. ) ;
#112397=PLANE ( 'NONE',  #143267 ) ;
#112510=EDGE_CURVE ( 'NONE', #41998, #35005, #54576, .T. ) ;
#113171=PLANE ( 'NONE',  #199074 ) ;
#113202=CARTESIAN_POINT ( 'NONE',  ( 2.400000000000000799, 0.000000000000000000, 0.000000000000000000 ) ) ;
#113480=SPHERICAL_SURFACE ( 'NONE', #122612, 4.324969328314201888 ) ;
#113527=DIRECTION ( 'NONE',  ( 0.000000000000000000, 0.000000000000000000, 1.000000000000000000 ) ) ;
#113674=DIRECTION ( 'NONE',  ( 1.000000000000000000, 0.000000000000000000, -0.000000000000000000 ) ) ;
#114157=DIRECTION ( 'NONE',  ( 0.000000000000000000, 0.000000000000000000, 1.000000000000000000 ) ) ;
#114377=FACE_BOUND ( 'NONE', #176269, .T. ) ;
#115402=DIRECTION ( 'NONE',  ( -0.000000000000000000, 0.000000000000000000, 1.000000000000000000 ) ) ;
#115475=VECTOR ( 'NONE', #11216, 1000.000000000000000 ) ;
#115586=ORIENTED_EDGE ( 'NONE', *, *, #88498, .T. ) ;
#115678=ORIENTED_EDGE ( 'NONE', *, *, #65894, .F. ) ;
#116067=DIRECTION ( 'NONE',  ( 0.000000000000000000, 0.000000000000000000, 1.000000000000000000 ) ) ;
#116252=ADVANCED_FACE ( 'NONE', ( #162997 ), #178182, .T. ) ;
#116264=AXIS2_PLACEMENT_3D ( 'NONE', #181549, #150216, #59169 ) ;
#116344=ORIENTED_EDGE ( 'NONE', *, *, #13078, .F. ) ;
#117109=ORIENTED_EDGE ( 'NONE', *, *, #122840, .F. ) ;
#117197=VERTEX_POINT ( 'NONE', #74972 ) ;
#117346=EDGE_LOOP ( 'NONE', ( #69129, #134531, #37224, #86570 ) ) ;
#117395=CARTESIAN_POINT ( 'NONE',  ( 1.300000000000000044, -0.7216878364870319418, 1.249999999999999778 ) ) ;
#117488=PLANE ( 'NONE',  #84904 ) ;
#117721=AXIS2_PLACEMENT_3D ( 'NONE', #15187, #63675, #124342 ) ;
#117795=CIRCLE ( 'NONE', #66083, 1.249999999999999778 ) ;
#117974=AXIS2_PLACEMENT_3D ( 'NONE', #186476, #79264, #97391 ) ;
#118657=FACE_OUTER_BOUND ( 'NONE', #4933, .T. ) ;
#118900=EDGE_CURVE ( 'NONE', #3247, #45202, #128025, .T. ) ;
#119193=DIRECTION ( 'NONE',  ( 0.000000000000000000, 0.000000000000000000, 1.000000000000000000 ) ) ;
#119500=EDGE_LOOP ( 'NONE', ( #75060, #6214 ) ) ;
#119780=CARTESIAN_POINT ( 'NONE',  ( 0.000000000000000000, 0.000000000000000000, 1.999999999999999112 ) ) ;
#119849=CARTESIAN_POINT ( 'NONE',  ( 2.200000000000000622, 1.999999999999999112, 0.000000000000000000 ) ) ;
#120001=VERTEX_POINT ( 'NONE', #161371 ) ;
#120106=DIRECTION ( 'NONE',  ( -1.000000000000000000, -0.000000000000000000, -0.000000000000000000 ) ) ;
#121040=EDGE_CURVE ( 'NONE', #83313, #54292, #58137, .T. ) ;
#121725=CARTESIAN_POINT ( 'NONE',  ( 2.200000000000000622, 0.000000000000000000, 0.000000000000000000 ) ) ;
#122226=DIRECTION ( 'NONE',  ( -1.000000000000000000, -0.000000000000000000, -0.000000000000000000 ) ) ;
#122612=AXIS2_PLACEMENT_3D ( 'NONE', #163002, #36640, #8323 ) ;
#122632=ORIENTED_EDGE ( 'NONE', *, *, #130384, .F. ) ;
#122788=CIRCLE ( 'NONE', #164817, 2.199999999999999289 ) ;
#122840=EDGE_CURVE ( 'NONE', #35005, #171876, #130417, .T. ) ;
#123014=ORIENTED_EDGE ( 'NONE', *, *, #136319, .T. ) ;
#123310=ORIENTED_EDGE ( 'NONE', *, *, #88498, .F. ) ;
#123639=ORIENTED_EDGE ( 'NONE', *, *, #99796, .T. ) ;
#124125=DIRECTION ( 'NONE',  ( -0.000000000000000000, 1.000000000000000000, -0.000000000000000000 ) ) ;
#124192=CIRCLE ( 'NONE', #137049, 3.799999999999999378 ) ;
#124342=DIRECTION ( 'NONE',  ( 0.000000000000000000, 0.000000000000000000, 1.000000000000000000 ) ) ;
#124651=ORIENTED_EDGE ( 'NONE', *, *, #14709, .F. ) ;
#124709=DIRECTION ( 'NONE',  ( 0.000000000000000000, 0.000000000000000000, 1.000000000000000000 ) ) ;
#124739=AXIS2_PLACEMENT_3D ( 'NONE', #153952, #16442, #135824 ) ;
#125460=CARTESIAN_POINT ( 'NONE',  ( 1.820000000000000062, 0.000000000000000000, 0.000000000000000000 ) ) ;
#126632=CARTESIAN_POINT ( 'NONE',  ( 1.300000000000000044, 0.7216878364870328300, -1.250000000000000000 ) ) ;
#127170=EDGE_LOOP ( 'NONE', ( #103912, #60489, #193059, #140234, #85488 ) ) ;
#127381=CIRCLE ( 'NONE', #53057, 0.2000000000000000944 ) ;
#127476=CIRCLE ( 'NONE', #4794, 1.249999999999999778 ) ;
#127705=DIRECTION ( 'NONE',  ( -1.000000000000000000, 0.000000000000000000, 0.000000000000000000 ) ) ;
#128025=LINE ( 'NONE', #186758, #67759 ) ;
#128168=EDGE_LOOP ( 'NONE', ( #32015, #123639, #136272, #64526, #112020 ) ) ;
#128371=CARTESIAN_POINT ( 'NONE',  ( 2.200000000000000178, 0.000000000000000000, 0.000000000000000000 ) ) ;
#128548=DIRECTION ( 'NONE',  ( 0.000000000000000000, 0.000000000000000000, 1.000000000000000000 ) ) ;
#128952=AXIS2_PLACEMENT_3D ( 'NONE', #136638, #181186, #71991 ) ;
#129249=EDGE_CURVE ( 'NONE', #13448, #171876, #23495, .T. ) ;
#129264=VECTOR ( 'NONE', #157286, 999.9999999999998863 ) ;
#129401=CARTESIAN_POINT ( 'NONE',  ( 1.300000000000000044, 0.7216878364870328300, 1.249999999999999778 ) ) ;
#129684=ADVANCED_FACE ( 'NONE', ( #161001 ), #113480, .T. ) ;
#129997=CARTESIAN_POINT ( 'NONE',  ( 1.300000000000000044, -0.7216878364870318308, 1.249999999999999778 ) ) ;
#130317=CARTESIAN_POINT ( 'NONE',  ( 1.300000000000000044, -0.7216878364870319418, 1.249999999999999778 ) ) ;
#130384=EDGE_CURVE ( 'NONE', #172465, #87119, #190306, .T. ) ;
#130417=LINE ( 'NONE', #52593, #28846 ) ;
#130550=LINE ( 'NONE', #52715, #52864 ) ;
#130742=ORIENTED_EDGE ( 'NONE', *, *, #170510, .F. ) ;
#130766=EDGE_LOOP ( 'NONE', ( #117109, #95511, #184232 ) ) ;
#131564=FACE_OUTER_BOUND ( 'NONE', #96641, .T. ) ;
#131782=CARTESIAN_POINT ( 'NONE',  ( 1.300000000000000044, -1.443375672974063884, -3.691112476943992763E-18 ) ) ;
#132028=LINE ( 'NONE', #129997, #140377 ) ;
#132186=AXIS2_PLACEMENT_3D ( 'NONE', #38494, #100150, #101141 ) ;
#132327=CIRCLE ( 'NONE', #35466, 3.799999999999999378 ) ;
#132538=ORIENTED_EDGE ( 'NONE', *, *, #73698, .T. ) ;
#132614=EDGE_CURVE ( 'NONE', #144758, #2854, #172855, .T. ) ;
#132903=PLANE ( 'NONE',  #33738 ) ;
#133049=ORIENTED_EDGE ( 'NONE', *, *, #110780, .F. ) ;
#133099=CARTESIAN_POINT ( 'NONE',  ( 0.000000000000000000, -0.7216878364870318308, -1.250000000000000000 ) ) ;
#133110=LINE ( 'NONE', #11794, #163818 ) ;
#133780=DIRECTION ( 'NONE',  ( 0.000000000000000000, 0.000000000000000000, 1.000000000000000000 ) ) ;
#133782=CARTESIAN_POINT ( 'NONE',  ( 10.20000000000000107, 0.000000000000000000, 1.610000000000000098 ) ) ;
#134090=EDGE_LOOP ( 'NONE', ( #171895, #135117, #12655 ) ) ;
#134313=DIRECTION ( 'NONE',  ( -1.000000000000000000, -0.000000000000000000, -0.000000000000000000 ) ) ;
#134343=FACE_OUTER_BOUND ( 'NONE', #97415, .T. ) ;
#134531=ORIENTED_EDGE ( 'NONE', *, *, #186207, .T. ) ;
#134636=DIRECTION ( 'NONE',  ( 0.000000000000000000, 0.000000000000000000, -1.000000000000000000 ) ) ;
#134698=DIRECTION ( 'NONE',  ( 0.000000000000000000, 0.8660254037844387076, -0.4999999999999999445 ) ) ;
#135117=ORIENTED_EDGE ( 'NONE', *, *, #45131, .F. ) ;
#135370=( NAMED_UNIT ( * ) SI_UNIT ( $, .STERADIAN. ) SOLID_ANGLE_UNIT ( ) );
#135435=EDGE_CURVE ( 'NONE', #84987, #171876, #62850, .T. ) ;
#135824=DIRECTION ( 'NONE',  ( 0.000000000000000000, -0.4999999999999998890, 0.8660254037844387076 ) ) ;
#136272=ORIENTED_EDGE ( 'NONE', *, *, #57708, .T. ) ;
#136319=EDGE_CURVE ( 'NONE', #182913, #191214, #169368, .T. ) ;
#136347=ORIENTED_EDGE ( 'NONE', *, *, #157667, .F. ) ;
#136544=DIRECTION ( 'NONE',  ( -1.000000000000000000, 0.000000000000000000, 0.000000000000000000 ) ) ;
#136638=CARTESIAN_POINT ( 'NONE',  ( 8.673617379884035472E-16, 0.000000000000000000, 0.000000000000000000 ) ) ;
#137049=AXIS2_PLACEMENT_3D ( 'NONE', #94878, #122226, #30230 ) ;
#137089=COLOUR_RGB ( '', 0.08235294, 0.09019608, 0.10196078) ;
#137481=EDGE_LOOP ( 'NONE', ( #55668, #37985, #61968, #39791 ) ) ;
#137680=EDGE_CURVE ( 'NONE', #83313, #16981, #41254, .T. ) ;
#137748=DIRECTION ( 'NONE',  ( -0.7071067811865492381, 0.000000000000000000, 0.7071067811865457964 ) ) ;
#137772=ORIENTED_EDGE ( 'NONE', *, *, #57273, .F. ) ;
#137787=FACE_OUTER_BOUND ( 'NONE', #168713, .T. ) ;
#137921=CARTESIAN_POINT ( 'NONE',  ( 0.000000000000000000, -1.443375672974063884, -3.691112476943992763E-18 ) ) ;
#138008=EDGE_LOOP ( 'NONE', ( #100237, #84415, #157411, #115586 ) ) ;
#138476=DIRECTION ( 'NONE',  ( -1.000000000000000000, -0.000000000000000000, -0.000000000000000000 ) ) ;
#138559=LINE ( 'NONE', #37, #176804 ) ;
#138611=CARTESIAN_POINT ( 'NONE',  ( 9.809999999999998721, 0.000000000000000000, 0.000000000000000000 ) ) ;
#138879=DIRECTION ( 'NONE',  ( -1.000000000000000000, 0.000000000000000000, 0.000000000000000000 ) ) ;
#139800=ORIENTED_EDGE ( 'NONE', *, *, #53832, .F. ) ;
#139801=ORIENTED_EDGE ( 'NONE', *, *, #132614, .T. ) ;
#139930=ORIENTED_EDGE ( 'NONE', *, *, #13078, .T. ) ;
#140046=AXIS2_PLACEMENT_3D ( 'NONE', #53728, #39552, #128548 ) ;
#140234=ORIENTED_EDGE ( 'NONE', *, *, #24149, .F. ) ;
#140289=EDGE_CURVE ( 'NONE', #185003, #117197, #124192, .T. ) ;
#140377=VECTOR ( 'NONE', #161366, 1000.000000000000000 ) ;
#140895=CIRCLE ( 'NONE', #176423, 1.249999999999999778 ) ;
#141287=CARTESIAN_POINT ( 'NONE',  ( 1.300000000000000044, -1.082531754730548412, 0.6249999999999998890 ) ) ;
#141333=ADVANCED_FACE ( 'NONE', ( #5842 ), #175880, .F. ) ;
#141424=UNCERTAINTY_MEASURE_WITH_UNIT (LENGTH_MEASURE( 1.000000000000000082E-05 ), #198021, 'distance_accuracy_value', 'NONE');
#141979=ORIENTED_EDGE ( 'NONE', *, *, #57708, .F. ) ;
#142010=ORIENTED_EDGE ( 'NONE', *, *, #71748, .F. ) ;
#142466=ORIENTED_EDGE ( 'NONE', *, *, #130384, .T. ) ;
#143072=AXIS2_PLACEMENT_3D ( 'NONE', #195350, #39647, #101308 ) ;
#143267=AXIS2_PLACEMENT_3D ( 'NONE', #21387, #83045, #115402 ) ;
#143393=AXIS2_PLACEMENT_3D ( 'NONE', #36, #107220, #93044 ) ;
#143394=PRODUCT_DEFINITION_CONTEXT ( 'detailed design', #174, 'design' ) ;
#143538=DIRECTION ( 'NONE',  ( -1.000000000000000000, -0.000000000000000000, -0.000000000000000000 ) ) ;
#143921=ORIENTED_EDGE ( 'NONE', *, *, #65570, .F. ) ;
#144022=CARTESIAN_POINT ( 'NONE',  ( 0.000000000000000000, 0.000000000000000000, 0.000000000000000000 ) ) ;
#144591=DIRECTION ( 'NONE',  ( -1.000000000000000000, -0.000000000000000000, -0.000000000000000000 ) ) ;
#144758=VERTEX_POINT ( 'NONE', #1718 ) ;
#144867=CARTESIAN_POINT ( 'NONE',  ( 1.820000000000000062, 3.799999999999999378, 0.000000000000000000 ) ) ;
#145016=CYLINDRICAL_SURFACE ( 'NONE', #89385, 3.799999999999999378 ) ;
#145579=DIRECTION ( 'NONE',  ( -0.000000000000000000, -0.5000000000000002220, 0.8660254037844384856 ) ) ;
#146015=PLANE ( 'NONE',  #47527 ) ;
#146350=DIRECTION ( 'NONE',  ( -0.000000000000000000, 0.5000000000000001110, 0.8660254037844385966 ) ) ;
#146529=DIRECTION ( 'NONE',  ( 1.000000000000000000, 0.000000000000000000, 0.000000000000000000 ) ) ;
#146590=DIRECTION ( 'NONE',  ( 0.000000000000000000, 0.000000000000000000, -1.000000000000000000 ) ) ;
#146780=PRODUCT_DEFINITION_SHAPE ( 'NONE', 'NONE',  #103014 ) ;
#146922=ORIENTED_EDGE ( 'NONE', *, *, #89104, .T. ) ;
#146986=DIRECTION ( 'NONE',  ( -1.000000000000000000, 0.000000000000000000, -0.000000000000000000 ) ) ;
#147124=DIRECTION ( 'NONE',  ( -1.000000000000000000, 0.000000000000000000, 0.000000000000000000 ) ) ;
#147218=AXIS2_PLACEMENT_3D ( 'NONE', #26619, #40775, #133780 ) ;
#147245=EDGE_CURVE ( 'NONE', #11758, #82858, #168253, .T. ) ;
#147258=AXIS2_PLACEMENT_3D ( 'NONE', #91772, #26170, #181837 ) ;
#147274=ORIENTED_EDGE ( 'NONE', *, *, #95409, .T. ) ;
#147678=CARTESIAN_POINT ( 'NONE',  ( 2.400000000000000799, 2.694222958124176020E-16, -2.199999999999999289 ) ) ;
#147681=COLOUR_RGB ( '', 0.08235294, 0.09019608, 0.10196078) ;
#148254=EDGE_LOOP ( 'NONE', ( #137772, #139801, #186471, #164184, #169281 ) ) ;
#149198=DIRECTION ( 'NONE',  ( -1.000000000000000000, 0.000000000000000000, -0.000000000000000000 ) ) ;
#149257=ORIENTED_EDGE ( 'NONE', *, *, #24149, .T. ) ;
#149477=VERTEX_POINT ( 'NONE', #196399 ) ;
#149526=FILL_AREA_STYLE ('',( #166698 ) ) ;
#149717=CARTESIAN_POINT ( 'NONE',  ( 1.300000000000000044, 0.7216878364870328300, 1.249999999999999778 ) ) ;
#149872=CARTESIAN_POINT ( 'NONE',  ( 1.300000000000000044, -0.7216878364870318308, -1.250000000000000000 ) ) ;
#150216=DIRECTION ( 'NONE',  ( -1.000000000000000000, -0.000000000000000000, -0.000000000000000000 ) ) ;
#150360=VERTEX_POINT ( 'NONE', #61806 ) ;
#150365=DIRECTION ( 'NONE',  ( -1.000000000000000000, 0.000000000000000000, 0.000000000000000000 ) ) ;
#150994=DIRECTION ( 'NONE',  ( 0.000000000000000000, 0.000000000000000000, -1.000000000000000000 ) ) ;
#151041=ORIENTED_EDGE ( 'NONE', *, *, #122840, .T. ) ;
#151195=PLANE ( 'NONE',  #37804 ) ;
#151354=LINE ( 'NONE', #25024, #198575 ) ;
#151519=CARTESIAN_POINT ( 'NONE',  ( 0.000000000000000000, 0.000000000000000000, 0.000000000000000000 ) ) ;
#151525=( LENGTH_UNIT ( ) NAMED_UNIT ( * ) SI_UNIT ( .MILLI., .METRE. ) );
#152231=ORIENTED_EDGE ( 'NONE', *, *, #20577, .T. ) ;
#152450=CARTESIAN_POINT ( 'NONE',  ( 0.000000000000000000, -1.443375672974063884, -3.691112476943992763E-18 ) ) ;
#152511=ADVANCED_FACE ( 'NONE', ( #118657 ), #11491, .T. ) ;
#152886=CARTESIAN_POINT ( 'NONE',  ( 0.000000000000000000, 0.7216878364870328300, 1.249999999999999778 ) ) ;
#153054=CARTESIAN_POINT ( 'NONE',  ( 1.300000000000000044, 1.443375672974065216, 7.017607234860990640E-28 ) ) ;
#153230=AXIS2_PLACEMENT_3D ( 'NONE', #87114, #58761, #45588 ) ;
#153329=VECTOR ( 'NONE', #79146, 1000.000000000000000 ) ;
#153443=DIRECTION ( 'NONE',  ( -0.000000000000000000, -0.4999999999999999445, -0.8660254037844387076 ) ) ;
#153494=SHAPE_DEFINITION_REPRESENTATION ( #146780, #71529 ) ;
#153952=CARTESIAN_POINT ( 'NONE',  ( 1.300000000000000044, -0.7216878364870318308, -1.250000000000000000 ) ) ;
#154401=EDGE_CURVE ( 'NONE', #149477, #84987, #34243, .T. ) ;
#154437=CARTESIAN_POINT ( 'NONE',  ( 1.300000000000000044, -0.7216878364870318308, -1.250000000000000000 ) ) ;
#154540=ADVANCED_FACE ( 'NONE', ( #134343 ), #198933, .F. ) ;
#154987=EDGE_LOOP ( 'NONE', ( #38353, #23666, #12330, #187844, #192434 ) ) ;
#157286=DIRECTION ( 'NONE',  ( -0.000000000000000000, -0.4999999999999999445, -0.8660254037844387076 ) ) ;
#157356=TOROIDAL_SURFACE ( 'NONE', #183203, 2.199999999999999289, 0.2000000000000000111 ) ;
#157393=DIRECTION ( 'NONE',  ( -1.000000000000000000, 0.000000000000000000, 0.000000000000000000 ) ) ;
#157411=ORIENTED_EDGE ( 'NONE', *, *, #147245, .T. ) ;
#157667=EDGE_CURVE ( 'NONE', #2854, #144758, #4921, .T. ) ;
#157983=DIRECTION ( 'NONE',  ( 0.000000000000000000, 0.000000000000000000, 1.000000000000000000 ) ) ;
#158394=ORIENTED_EDGE ( 'NONE', *, *, #118900, .T. ) ;
#158408=CARTESIAN_POINT ( 'NONE',  ( 3.885274725274726393, -8.673617379884035472E-16, 0.000000000000000000 ) ) ;
#158680=CARTESIAN_POINT ( 'NONE',  ( 2.400000000000000799, 0.000000000000000000, 0.000000000000000000 ) ) ;
#159084=VERTEX_POINT ( 'NONE', #152886 ) ;
#159091=AXIS2_PLACEMENT_3D ( 'NONE', #138611, #27500, #15283 ) ;
#159559=CARTESIAN_POINT ( 'NONE',  ( 10.20000000000000107, 0.000000000000000000, 0.000000000000000000 ) ) ;
#160275=ORIENTED_EDGE ( 'NONE', *, *, #9184, .F. ) ;
#160405=DIRECTION ( 'NONE',  ( 0.000000000000000000, 1.000000000000000000, 1.224646799147353207E-16 ) ) ;
#160525=AXIS2_PLACEMENT_3D ( 'NONE', #130317, #192014, #114157 ) ;
#161001=FACE_OUTER_BOUND ( 'NONE', #128168, .T. ) ;
#161113=DIRECTION ( 'NONE',  ( -0.000000000000000000, -0.4999999999999999445, -0.8660254037844387076 ) ) ;
#161366=DIRECTION ( 'NONE',  ( -0.000000000000000000, -1.000000000000000000, -0.000000000000000000 ) ) ;
#161371=CARTESIAN_POINT ( 'NONE',  ( 1.300000000000000044, 0.000000000000000000, -1.250000000000000000 ) ) ;
#161515=VERTEX_POINT ( 'NONE', #196390 ) ;
#161920=CARTESIAN_POINT ( 'NONE',  ( 2.200000000000000622, 0.000000000000000000, 0.000000000000000000 ) ) ;
#162181=DIRECTION ( 'NONE',  ( -1.000000000000000000, 0.000000000000000000, 0.000000000000000000 ) ) ;
#162240=DIRECTION ( 'NONE',  ( 0.000000000000000000, -0.5000000000000001110, -0.8660254037844385966 ) ) ;
#162401=VECTOR ( 'NONE', #124125, 1000.000000000000000 ) ;
#162564=EDGE_CURVE ( 'NONE', #83320, #100314, #60809, .T. ) ;
#162997=FACE_OUTER_BOUND ( 'NONE', #127170, .T. ) ;
#163002=CARTESIAN_POINT ( 'NONE',  ( 3.885274725274726393, -8.673617379884035472E-16, 0.000000000000000000 ) ) ;
#163018=FACE_OUTER_BOUND ( 'NONE', #21113, .T. ) ;
#163074=PRODUCT_DEFINITION_FORMATION_WITH_SPECIFIED_SOURCE ( 'ANY', '', #177482, .NOT_KNOWN. ) ;
#163374=CARTESIAN_POINT ( 'NONE',  ( 0.000000000000000000, 0.7216878364870328300, -1.250000000000000000 ) ) ;
#163392=VECTOR ( 'NONE', #52925, 1000.000000000000000 ) ;
#163628=VERTEX_POINT ( 'NONE', #196152 ) ;
#163818=VECTOR ( 'NONE', #196805, 1000.000000000000000 ) ;
#164184=ORIENTED_EDGE ( 'NONE', *, *, #140289, .F. ) ;
#164817=AXIS2_PLACEMENT_3D ( 'NONE', #121725, #46884, #124709 ) ;
#164825=CARTESIAN_POINT ( 'NONE',  ( 1.300000000000000044, 1.082531754730548856, -0.6250000000000003331 ) ) ;
#165670=DIRECTION ( 'NONE',  ( 0.000000000000000000, 0.000000000000000000, 1.000000000000000000 ) ) ;
#165918=AXIS2_PLACEMENT_3D ( 'NONE', #117395, #136544, #87059 ) ;
#165964=DIRECTION ( 'NONE',  ( 0.000000000000000000, -1.000000000000000000, 0.000000000000000000 ) ) ;
#166302=AXIS2_PLACEMENT_3D ( 'NONE', #33802, #64144, #66119 ) ;
#166698=FILL_AREA_STYLE_COLOUR ( '', #137089 ) ;
#166995=VERTEX_POINT ( 'NONE', #164825 ) ;
#167140=EDGE_CURVE ( 'NONE', #11758, #16981, #102322, .T. ) ;
#167632=LINE ( 'NONE', #152450, #38115 ) ;
#167684=PRODUCT_CONTEXT ( 'NONE', #183562, 'mechanical' ) ;
#168253=LINE ( 'NONE', #119780, #47094 ) ;
#168590=VERTEX_POINT ( 'NONE', #38944 ) ;
#168713=EDGE_LOOP ( 'NONE', ( #25227, #73874, #59004, #87847, #40568 ) ) ;
#169037=ORIENTED_EDGE ( 'NONE', *, *, #14709, .T. ) ;
#169227=ADVANCED_FACE ( 'NONE', ( #23783 ), #24794, .T. ) ;
#169250=AXIS2_PLACEMENT_3D ( 'NONE', #17675, #96474, #80316 ) ;
#169281=ORIENTED_EDGE ( 'NONE', *, *, #99796, .F. ) ;
#169368=CIRCLE ( 'NONE', #30542, 0.2000000000000000944 ) ;
#169434=VECTOR ( 'NONE', #15931, 1000.000000000000114 ) ;
#169591=CARTESIAN_POINT ( 'NONE',  ( 0.000000000000000000, 0.000000000000000000, 0.000000000000000000 ) ) ;
#169719=EDGE_LOOP ( 'NONE', ( #18792, #23367, #55953, #124651, #68895 ) ) ;
#169869=VERTEX_POINT ( 'NONE', #149872 ) ;
#170510=EDGE_CURVE ( 'NONE', #159084, #8650, #138559, .T. ) ;
#171876=VERTEX_POINT ( 'NONE', #90246 ) ;
#171895=ORIENTED_EDGE ( 'NONE', *, *, #39003, .F. ) ;
#172107=DIRECTION ( 'NONE',  ( -1.000000000000000000, -0.000000000000000000, -0.000000000000000000 ) ) ;
#172465=VERTEX_POINT ( 'NONE', #21944 ) ;
#172855=CIRCLE ( 'NONE', #30398, 3.799999999999999378 ) ;
#172887=VECTOR ( 'NONE', #27642, 1000.000000000000000 ) ;
#173030=EDGE_CURVE ( 'NONE', #168590, #166995, #133110, .T. ) ;
#173162=LINE ( 'NONE', #126632, #153329 ) ;
#173277=ORIENTED_EDGE ( 'NONE', *, *, #154401, .F. ) ;
#173760=EDGE_LOOP ( 'NONE', ( #142010, #6478, #147274, #96593, #105926 ) ) ;
#173877=DIRECTION ( 'NONE',  ( 0.000000000000000000, 0.000000000000000000, 1.000000000000000000 ) ) ;
#174055=CARTESIAN_POINT ( 'NONE',  ( 0.000000000000000000, 0.7216878364870328300, -1.250000000000000000 ) ) ;
#174234=CARTESIAN_POINT ( 'NONE',  ( 1.300000000000000044, -0.7216878364870319418, 1.249999999999999778 ) ) ;
#174302=LINE ( 'NONE', #35771, #163392 ) ;
#174380=LINE ( 'NONE', #54535, #99023 ) ;
#174588=FACE_OUTER_BOUND ( 'NONE', #119500, .T. ) ;
#174858=DIRECTION ( 'NONE',  ( 1.000000000000000000, 0.000000000000000000, 0.000000000000000000 ) ) ;
#174899=EDGE_CURVE ( 'NONE', #169869, #163628, #84324, .T. ) ;
#175859=FACE_OUTER_BOUND ( 'NONE', #134090, .T. ) ;
#175880=CONICAL_SURFACE ( 'NONE', #192037, 1732.050807568856271, 1.047197551196592524 ) ;
#176026=AXIS2_PLACEMENT_3D ( 'NONE', #159559, #69562, #116067 ) ;
#176269=EDGE_LOOP ( 'NONE', ( #189471, #108486, #47313, #169037, #61713, #149257 ) ) ;
#176379=FACE_OUTER_BOUND ( 'NONE', #169719, .T. ) ;
#176423=AXIS2_PLACEMENT_3D ( 'NONE', #67906, #172107, #33593 ) ;
#176804=VECTOR ( 'NONE', #18223, 1000.000000000000000 ) ;
#177482=PRODUCT ( 'socket button head screw_iso_ISO 7380 - M4 x 8 - 8N', 'socket button head screw_iso_ISO 7380 - M4 x 8 - 8N', '', ( #167684 ) ) ;
#178064=PRESENTATION_STYLE_ASSIGNMENT (( #190227 ) ) ;
#178083=DIRECTION ( 'NONE',  ( -1.000000000000000000, -0.000000000000000000, -0.000000000000000000 ) ) ;
#178182=PLANE ( 'NONE',  #143072 ) ;
#178187=DIRECTION ( 'NONE',  ( -0.5000000000000044409, 0.000000000000000000, 0.8660254037844360431 ) ) ;
#178622=LINE ( 'NONE', #133099, #38253 ) ;
#178775=CARTESIAN_POINT ( 'NONE',  ( 10.20000000000000107, 1.971681346627238735E-16, -1.610000000000000098 ) ) ;
#178825=AXIS2_PLACEMENT_3D ( 'NONE', #174234, #127705, #113527 ) ;
#178881=PRESENTATION_STYLE_ASSIGNMENT (( #28201 ) ) ;
#178993=VECTOR ( 'NONE', #146350, 1000.000000000000000 ) ;
#179038=EDGE_LOOP ( 'NONE', ( #103415, #55818, #87077 ) ) ;
#179185=CARTESIAN_POINT ( 'NONE',  ( 1.300000000000000044, -0.7216878364870319418, 1.249999999999999778 ) ) ;
#179815=ORIENTED_EDGE ( 'NONE', *, *, #75719, .F. ) ;
#180036=VECTOR ( 'NONE', #137748, 1000.000000000000000 ) ;
#180107=ORIENTED_EDGE ( 'NONE', *, *, #186506, .F. ) ;
#180891=ORIENTED_EDGE ( 'NONE', *, *, #90570, .T. ) ;
#181186=DIRECTION ( 'NONE',  ( -1.000000000000000000, -0.000000000000000000, -0.000000000000000000 ) ) ;
#181549=CARTESIAN_POINT ( 'NONE',  ( 10.20000000000000107, 0.000000000000000000, 0.000000000000000000 ) ) ;
#181796=DIRECTION ( 'NONE',  ( 0.000000000000000000, 0.000000000000000000, 1.000000000000000000 ) ) ;
#181837=DIRECTION ( 'NONE',  ( 0.000000000000000000, 0.000000000000000000, 1.000000000000000000 ) ) ;
#182078=CIRCLE ( 'NONE', #7693, 3.799999999999999378 ) ;
#182253=ORIENTED_EDGE ( 'NONE', *, *, #29688, .F. ) ;
#182292=CARTESIAN_POINT ( 'NONE',  ( 9.809999999999998721, 2.449293598294705921E-16, -1.999999999999999556 ) ) ;
#182852=FACE_OUTER_BOUND ( 'NONE', #148254, .T. ) ;
#182858=( NAMED_UNIT ( * ) PLANE_ANGLE_UNIT ( ) SI_UNIT ( $, .RADIAN. ) );
#182913=VERTEX_POINT ( 'NONE', #105896 ) ;
#183121=ORIENTED_EDGE ( 'NONE', *, *, #135435, .F. ) ;
#183203=AXIS2_PLACEMENT_3D ( 'NONE', #79790, #138476, #200157 ) ;
#183333=ORIENTED_EDGE ( 'NONE', *, *, #61495, .T. ) ;
#183435=DIRECTION ( 'NONE',  ( -1.000000000000000000, -0.000000000000000000, -0.000000000000000000 ) ) ;
#183562=APPLICATION_CONTEXT ( 'automotive_design' ) ;
#184232=ORIENTED_EDGE ( 'NONE', *, *, #95409, .F. ) ;
#185003=VERTEX_POINT ( 'NONE', #84494 ) ;
#185178=ADVANCED_FACE ( 'NONE', ( #89505, #198682 ), #151195, .F. ) ;
#185756=AXIS2_PLACEMENT_3D ( 'NONE', #82546, #23898, #85551 ) ;
#185943=EDGE_LOOP ( 'NONE', ( #77748, #37588, #3021, #139800, #143921 ) ) ;
#186207=EDGE_CURVE ( 'NONE', #16981, #191214, #174302, .T. ) ;
#186332=AXIS2_PLACEMENT_3D ( 'NONE', #43466, #102142, #25328 ) ;
#186471=ORIENTED_EDGE ( 'NONE', *, *, #65570, .T. ) ;
#186476=CARTESIAN_POINT ( 'NONE',  ( 2.200000000000000178, 0.000000000000000000, 0.000000000000000000 ) ) ;
#186506=EDGE_CURVE ( 'NONE', #84987, #3247, #6418, .T. ) ;
#186758=CARTESIAN_POINT ( 'NONE',  ( 1.300000000000000044, -1.443375672974063884, -3.691112476943992763E-18 ) ) ;
#186823=ADVANCED_FACE ( 'NONE', ( #59910 ), #189226, .T. ) ;
#187844=ORIENTED_EDGE ( 'NONE', *, *, #162564, .F. ) ;
#188569=CARTESIAN_POINT ( 'NONE',  ( 1.300000000000000044, 1.443375672974065216, 7.017607234860990640E-28 ) ) ;
#189226=CONICAL_SURFACE ( 'NONE', #147218, 1.610000000000000098, 0.7853981633974458365 ) ;
#189471=ORIENTED_EDGE ( 'NONE', *, *, #170510, .T. ) ;
#189672=( GEOMETRIC_REPRESENTATION_CONTEXT ( 3 ) GLOBAL_UNCERTAINTY_ASSIGNED_CONTEXT ( ( #23637 ) ) GLOBAL_UNIT_ASSIGNED_CONTEXT ( ( #54703, #22377, #53710 ) ) REPRESENTATION_CONTEXT ( 'NONE', 'WORKASPACE' ) );
#189850=ADVANCED_FACE ( 'NONE', ( #58438 ), #46251, .T. ) ;
#190227=SURFACE_STYLE_USAGE ( .BOTH. , #24390 ) ;
#190306=CIRCLE ( 'NONE', #128952, 1.899999999999999689 ) ;
#191036=ORIENTED_EDGE ( 'NONE', *, *, #89104, .F. ) ;
#191114=CARTESIAN_POINT ( 'NONE',  ( 3.885274725274726393, -8.673617379884035472E-16, 0.000000000000000000 ) ) ;
#191214=VERTEX_POINT ( 'NONE', #81190 ) ;
#191516=CARTESIAN_POINT ( 'NONE',  ( 1.300000000000000044, -0.7216878364870318308, -1.250000000000000000 ) ) ;
#191528=FACE_OUTER_BOUND ( 'NONE', #185943, .T. ) ;
#192014=DIRECTION ( 'NONE',  ( -1.000000000000000000, 0.000000000000000000, 0.000000000000000000 ) ) ;
#192037=AXIS2_PLACEMENT_3D ( 'NONE', #66525, #85680, #97831 ) ;
#192247=CARTESIAN_POINT ( 'NONE',  ( 1.820000000000000062, 0.000000000000000000, 0.000000000000000000 ) ) ;
#192434=ORIENTED_EDGE ( 'NONE', *, *, #29924, .F. ) ;
#192610=CARTESIAN_POINT ( 'NONE',  ( 10.20000000000000107, 0.000000000000000000, 0.000000000000000000 ) ) ;
#192677=AXIS2_PLACEMENT_3D ( 'NONE', #85433, #147124, #193636 ) ;
#193059=ORIENTED_EDGE ( 'NONE', *, *, #75719, .T. ) ;
#193116=DIRECTION ( 'NONE',  ( 0.000000000000000000, 1.000000000000000000, 0.000000000000000000 ) ) ;
#193636=DIRECTION ( 'NONE',  ( 0.000000000000000000, 0.000000000000000000, 1.000000000000000000 ) ) ;
#193866=ORIENTED_EDGE ( 'NONE', *, *, #14429, .T. ) ;
#194053=( NAMED_UNIT ( * ) SI_UNIT ( $, .STERADIAN. ) SOLID_ANGLE_UNIT ( ) );
#194614=FACE_OUTER_BOUND ( 'NONE', #137481, .T. ) ;
#194656=ADVANCED_FACE ( 'NONE', ( #4353 ), #66038, .T. ) ;
#194693=VERTEX_POINT ( 'NONE', #144867 ) ;
#194788=DIRECTION ( 'NONE',  ( -0.000000000000000000, 0.4999999999999998890, -0.8660254037844387076 ) ) ;
#195350=CARTESIAN_POINT ( 'NONE',  ( 1.300000000000000044, 0.7216878364870328300, 1.249999999999999778 ) ) ;
#196026=DIRECTION ( 'NONE',  ( -1.000000000000000000, -0.000000000000000000, -0.000000000000000000 ) ) ;
#196152=CARTESIAN_POINT ( 'NONE',  ( 0.000000000000000000, -0.7216878364870318308, -1.250000000000000000 ) ) ;
#196390=CARTESIAN_POINT ( 'NONE',  ( 2.200000000000000622, 0.000000000000000000, 2.199999999999999289 ) ) ;
#196399=CARTESIAN_POINT ( 'NONE',  ( 1.300000000000000044, -1.082531754730548412, -0.6249999999999997780 ) ) ;
#196735=ORIENTED_EDGE ( 'NONE', *, *, #71748, .T. ) ;
#196805=DIRECTION ( 'NONE',  ( -0.000000000000000000, 0.5000000000000001110, 0.8660254037844385966 ) ) ;
#197689=ADVANCED_FACE ( 'NONE', ( #34569, #114377 ), #112397, .T. ) ;
#198021=( LENGTH_UNIT ( ) NAMED_UNIT ( * ) SI_UNIT ( .MILLI., .METRE. ) );
#198234=TOROIDAL_SURFACE ( 'NONE', #140046, 2.199999999999999289, 0.2000000000000000111 ) ;
#198494=ORIENTED_EDGE ( 'NONE', *, *, #9184, .T. ) ;
#198575=VECTOR ( 'NONE', #150365, 1000.000000000000000 ) ;
#198682=FACE_OUTER_BOUND ( 'NONE', #22950, .T. ) ;
#198933=CONICAL_SURFACE ( 'NONE', #24598, 1732.050807568856271, 1.047197551196592524 ) ;
#199074=AXIS2_PLACEMENT_3D ( 'NONE', #79862, #34358, #173877 ) ;
#199302=DIRECTION ( 'NONE',  ( -0.000000000000000000, -0.5000000000000002220, 0.8660254037844384856 ) ) ;
#199678=CARTESIAN_POINT ( 'NONE',  ( 1.300000000000000044, 1.082531754730548856, 0.6250000000000006661 ) ) ;
#200157=DIRECTION ( 'NONE',  ( 0.000000000000000000, 0.000000000000000000, 1.000000000000000000 ) ) ;
ENDSEC;
END-ISO-10303-21;
